ISO-10303-21;
HEADER;
FILE_DESCRIPTION (('STEP AP214'),
    '1' );
FILE_NAME ('socket head cap screw_iso_ISO 4762 M6 x 30 - 30N.step',
    '2026-09-21T15:58:29',
    ( '' ),
    ( '' ),
    'SwSTEP 2.0',
    'SolidWorks 2026',
    '' );
FILE_SCHEMA (( 'AUTOMOTIVE_DESIGN' ));
ENDSEC;

DATA;
#152=ORIENTED_EDGE ( 'NONE', *, *, #34112, .F. ) ;
#187=ADVANCED_FACE ( 'NONE', ( #3211 ), #1327, .T. ) ;
#201=ADVANCED_FACE ( 'NONE', ( #30385 ), #30581, .F. ) ;
#202=DIRECTION ( 'NONE',  ( 0.000000000000000000, 0.000000000000000000, -1.000000000000000000 ) ) ;
#345=AXIS2_PLACEMENT_3D ( 'NONE', #12956, #10173, #16343 ) ;
#346=CARTESIAN_POINT ( 'NONE',  ( 35.99999999999999289, 0.000000000000000000, 0.000000000000000000 ) ) ;
#388=CARTESIAN_POINT ( 'NONE',  ( 3.000000000000000000, 0.000000000000000000, 0.000000000000000000 ) ) ;
#401=VECTOR ( 'NONE', #13709, 1000.000000000000000 ) ;
#404=EDGE_CURVE ( 'NONE', #30547, #29314, #28481, .T. ) ;
#451=CARTESIAN_POINT ( 'NONE',  ( 6.249999999999998224, 0.000000000000000000, -3.250000000000001332 ) ) ;
#483=CARTESIAN_POINT ( 'NONE',  ( 35.99999999999999289, 0.000000000000000000, 2.445500000000000007 ) ) ;
#548=PLANE ( 'NONE',  #20272 ) ;
#627=EDGE_CURVE ( 'NONE', #19009, #36783, #8211, .T. ) ;
#685=DIRECTION ( 'NONE',  ( 0.000000000000000000, 0.000000000000000000, 1.000000000000000000 ) ) ;
#720=( NAMED_UNIT ( * ) SI_UNIT ( $, .STERADIAN. ) SOLID_ANGLE_UNIT ( ) );
#724=DIRECTION ( 'NONE',  ( 0.000000000000000000, -1.034244904716769672E-15, -1.000000000000000000 ) ) ;
#765=ORIENTED_EDGE ( 'NONE', *, *, #33305, .T. ) ;
#1013=VECTOR ( 'NONE', #2939, 1000.000000000000000 ) ;
#1015=DIRECTION ( 'NONE',  ( 0.000000000000000000, -0.5000000000000013323, -0.8660254037844379305 ) ) ;
#1106=TOROIDAL_SURFACE ( 'NONE', #22662, 4.700000000000000178, 0.2999999999999999889 ) ;
#1136=CARTESIAN_POINT ( 'NONE',  ( 4.467624384280048488, 0.000000000000000000, 0.000000000000000000 ) ) ;
#1232=CARTESIAN_POINT ( 'NONE',  ( -31.74999999999995737, 0.000000000000000000, 0.000000000000000000 ) ) ;
#1269=ORIENTED_EDGE ( 'NONE', *, *, #404, .F. ) ;
#1284=SHAPE_REPRESENTATION_RELATIONSHIP ( 'NONE' , 'NONE' ,  #22738, #4968 ) ;
#1327=PLANE ( 'NONE',  #4339 ) ;
#1345=CIRCLE ( 'NONE', #5555, 5.000000000000000000 ) ;
#1363=ORIENTED_EDGE ( 'NONE', *, *, #19027, .T. ) ;
#1485=CARTESIAN_POINT ( 'NONE',  ( 3.000000000000000000, 0.000000000000000000, 0.000000000000000000 ) ) ;
#1487=ORIENTED_EDGE ( 'NONE', *, *, #33305, .F. ) ;
#1654=AXIS2_PLACEMENT_3D ( 'NONE', #21908, #16119, #17845 ) ;
#1945=CARTESIAN_POINT ( 'NONE',  ( 35.99999999999999289, 2.994873747314852478E-16, -2.445500000000000007 ) ) ;
#1959=VERTEX_POINT ( 'NONE', #36563 ) ;
#1995=PRODUCT_DEFINITION ( 'UNKNOWN', '', #20147, #30919 ) ;
#2003=ORIENTED_EDGE ( 'NONE', *, *, #17646, .T. ) ;
#2021=CARTESIAN_POINT ( 'NONE',  ( 3.000000000000000000, -1.467624384280027172, 2.542000000000001592 ) ) ;
#2101=CONICAL_SURFACE ( 'NONE', #24235, 2.445500000000000007, 0.7853981633974749244 ) ;
#2159=( GEOMETRIC_REPRESENTATION_CONTEXT ( 3 ) GLOBAL_UNCERTAINTY_ASSIGNED_CONTEXT ( ( #24947 ) ) GLOBAL_UNIT_ASSIGNED_CONTEXT ( ( #19503, #33946, #720 ) ) REPRESENTATION_CONTEXT ( 'NONE', 'WORKASPACE' ) );
#2170=DIRECTION ( 'NONE',  ( 0.000000000000000000, 1.000000000000000000, -1.625241993126352989E-15 ) ) ;
#2171=CARTESIAN_POINT ( 'NONE',  ( 3.000000000000000000, -1.467624384280027172, 2.542000000000001592 ) ) ;
#2432=DIRECTION ( 'NONE',  ( 0.000000000000000000, 0.000000000000000000, 1.000000000000000000 ) ) ;
#2491=VERTEX_POINT ( 'NONE', #483 ) ;
#2512=LINE ( 'NONE', #7579, #2605 ) ;
#2558=ORIENTED_EDGE ( 'NONE', *, *, #23004, .T. ) ;
#2605=VECTOR ( 'NONE', #4948, 1000.000000000000114 ) ;
#2648=EDGE_CURVE ( 'NONE', #1959, #34152, #7676, .T. ) ;
#2662=DIRECTION ( 'NONE',  ( 0.000000000000000000, 0.000000000000000000, -1.000000000000000000 ) ) ;
#2687=VERTEX_POINT ( 'NONE', #16399 ) ;
#2699=AXIS2_PLACEMENT_3D ( 'NONE', #17771, #17580, #14584 ) ;
#2717=CARTESIAN_POINT ( 'NONE',  ( 3.000000000000000000, 2.935248768560057453, -3.903127820947815962E-15 ) ) ;
#2800=DIRECTION ( 'NONE',  ( 1.000000000000000000, 0.000000000000000000, 0.000000000000000000 ) ) ;
#2804=DIRECTION ( 'NONE',  ( 0.000000000000000000, 0.8660254037844380415, -0.5000000000000012212 ) ) ;
#2898=ORIENTED_EDGE ( 'NONE', *, *, #28312, .F. ) ;
#2939=DIRECTION ( 'NONE',  ( -1.000000000000000000, -0.000000000000000000, -0.000000000000000000 ) ) ;
#2992=DIRECTION ( 'NONE',  ( 0.000000000000000000, -0.5000000000000011102, -0.8660254037844379305 ) ) ;
#3034=DIRECTION ( 'NONE',  ( 0.000000000000000000, -0.4999999999999996114, 0.8660254037844388186 ) ) ;
#3191=ORIENTED_EDGE ( 'NONE', *, *, #5240, .T. ) ;
#3211=FACE_OUTER_BOUND ( 'NONE', #31371, .T. ) ;
#3318=CARTESIAN_POINT ( 'NONE',  ( 0.000000000000000000, 0.000000000000000000, 0.000000000000000000 ) ) ;
#3370=ADVANCED_FACE ( 'NONE', ( #8639 ), #25893, .F. ) ;
#3378=AXIS2_PLACEMENT_3D ( 'NONE', #6634, #5907, #26328 ) ;
#3491=CIRCLE ( 'NONE', #11269, 4.700000000000000178 ) ;
#3516=PRODUCT_CONTEXT ( 'NONE', #17321, 'mechanical' ) ;
#3559=VERTEX_POINT ( 'NONE', #25141 ) ;
#3627=ORIENTED_EDGE ( 'NONE', *, *, #11949, .T. ) ;
#3631=DIRECTION ( 'NONE',  ( 0.000000000000000000, 0.4999999999999991118, -0.8660254037844391517 ) ) ;
#3751=VERTEX_POINT ( 'NONE', #8431 ) ;
#3783=( NAMED_UNIT ( * ) SI_UNIT ( $, .STERADIAN. ) SOLID_ANGLE_UNIT ( ) );
#3902=( NAMED_UNIT ( * ) SI_UNIT ( $, .STERADIAN. ) SOLID_ANGLE_UNIT ( ) );
#4065=DIRECTION ( 'NONE',  ( -1.000000000000000000, -0.000000000000000000, -0.000000000000000000 ) ) ;
#4179=SURFACE_SIDE_STYLE ('',( #32085 ) ) ;
#4213=CARTESIAN_POINT ( 'NONE',  ( 35.44550000000001688, 0.000000000000000000, 0.000000000000000000 ) ) ;
#4249=CARTESIAN_POINT ( 'NONE',  ( 0.3000000000000016542, 0.000000000000000000, 5.000000000000000000 ) ) ;
#4339=AXIS2_PLACEMENT_3D ( 'NONE', #27390, #27014, #7509 ) ;
#4352=EDGE_LOOP ( 'NONE', ( #26010, #33318 ) ) ;
#4409=CARTESIAN_POINT ( 'NONE',  ( 3.000000000000000000, 2.201436576420041202, -1.271000000000003460 ) ) ;
#4516=ORIENTED_EDGE ( 'NONE', *, *, #19956, .F. ) ;
#4526=CIRCLE ( 'NONE', #30874, 2.541999999999999815 ) ;
#4574=CARTESIAN_POINT ( 'NONE',  ( 6.249999999999998224, 0.000000000000000000, 0.000000000000000000 ) ) ;
#4576=EDGE_CURVE ( 'NONE', #8984, #34090, #4526, .T. ) ;
#4586=AXIS2_PLACEMENT_3D ( 'NONE', #9701, #30508, #27675 ) ;
#4740=CARTESIAN_POINT ( 'NONE',  ( 3.000000000000000000, -2.629050547790028157E-15, -2.541999999999999815 ) ) ;
#4750=PLANE ( 'NONE',  #29789 ) ;
#4767=ORIENTED_EDGE ( 'NONE', *, *, #4576, .F. ) ;
#4792=ORIENTED_EDGE ( 'NONE', *, *, #32232, .T. ) ;
#4909=FACE_OUTER_BOUND ( 'NONE', #20654, .T. ) ;
#4948=DIRECTION ( 'NONE',  ( -0.5000000000000051070, 0.000000000000000000, 0.8660254037844355990 ) ) ;
#4968=ADVANCED_BREP_SHAPE_REPRESENTATION ( '', ( #19278, #21385 ), #2159 ) ;
#5070=DIRECTION ( 'NONE',  ( 0.000000000000000000, 0.000000000000000000, -1.000000000000000000 ) ) ;
#5076=PLANE ( 'NONE',  #20773 ) ;
#5240=EDGE_CURVE ( 'NONE', #14355, #7880, #24358, .T. ) ;
#5263=CARTESIAN_POINT ( 'NONE',  ( 0.000000000000000000, -1.467624384280027172, 2.542000000000001592 ) ) ;
#5286=CARTESIAN_POINT ( 'NONE',  ( 0.3000000000000016542, 0.000000000000000000, 0.000000000000000000 ) ) ;
#5331=CONICAL_SURFACE ( 'NONE', #25087, 2.445500000000000007, 0.7853981633974749244 ) ;
#5389=ORIENTED_EDGE ( 'NONE', *, *, #33729, .T. ) ;
#5413=CARTESIAN_POINT ( 'NONE',  ( 3.000000000000000000, -2.201436576420042979, 1.271000000000003682 ) ) ;
#5441=PLANE ( 'NONE',  #7126 ) ;
#5449=DIRECTION ( 'NONE',  ( -0.000000000000000000, 1.625241993126352989E-15, 1.000000000000000000 ) ) ;
#5502=DIRECTION ( 'NONE',  ( 0.000000000000000000, 0.4999999999999991118, -0.8660254037844391517 ) ) ;
#5555=AXIS2_PLACEMENT_3D ( 'NONE', #5286, #22886, #16721 ) ;
#5569=VECTOR ( 'NONE', #31697, 1000.000000000000000 ) ;
#5580=CARTESIAN_POINT ( 'NONE',  ( 0.3000000000000016542, 0.000000000000000000, 0.000000000000000000 ) ) ;
#5593=CARTESIAN_POINT ( 'NONE',  ( 3.000000000000000000, 0.000000000000000000, 0.000000000000000000 ) ) ;
#5600=DIRECTION ( 'NONE',  ( 0.000000000000000000, 0.000000000000000000, -1.000000000000000000 ) ) ;
#5604=CARTESIAN_POINT ( 'NONE',  ( 3.000000000000000000, -1.467624384280027172, 2.542000000000001592 ) ) ;
#5624=FACE_OUTER_BOUND ( 'NONE', #20039, .T. ) ;
#5683=VECTOR ( 'NONE', #28276, 1000.000000000000000 ) ;
#5701=VECTOR ( 'NONE', #34293, 1000.000000000000000 ) ;
#5762=ADVANCED_FACE ( 'NONE', ( #30707 ), #22074, .T. ) ;
#5799=PLANE ( 'NONE',  #30230 ) ;
#5803=VERTEX_POINT ( 'NONE', #28091 ) ;
#5804=UNCERTAINTY_MEASURE_WITH_UNIT (LENGTH_MEASURE( 1.000000000000000082E-05 ), #29293, 'distance_accuracy_value', 'NONE');
#5827=DIRECTION ( 'NONE',  ( 0.000000000000000000, 0.000000000000000000, -1.000000000000000000 ) ) ;
#5907=DIRECTION ( 'NONE',  ( -1.000000000000000000, -0.000000000000000000, -0.000000000000000000 ) ) ;
#5994=CIRCLE ( 'NONE', #27565, 2.541999999999999815 ) ;
#6133=PLANE ( 'NONE',  #19646 ) ;
#6331=ORIENTED_EDGE ( 'NONE', *, *, #2648, .F. ) ;
#6393=FACE_OUTER_BOUND ( 'NONE', #12162, .T. ) ;
#6401=EDGE_LOOP ( 'NONE', ( #35869, #23628, #27979, #36185 ) ) ;
#6423=ORIENTED_EDGE ( 'NONE', *, *, #34988, .T. ) ;
#6461=EDGE_CURVE ( 'NONE', #17975, #36602, #34965, .T. ) ;
#6472=DIRECTION ( 'NONE',  ( -1.000000000000000000, -0.000000000000000000, -0.000000000000000000 ) ) ;
#6550=CARTESIAN_POINT ( 'NONE',  ( 6.000000000000000000, 5.000000000000000000, 0.000000000000000000 ) ) ;
#6552=DIRECTION ( 'NONE',  ( 0.000000000000000000, 1.000000000000000000, -1.034244904716769672E-15 ) ) ;
#6634=CARTESIAN_POINT ( 'NONE',  ( 35.99999999999999289, 0.000000000000000000, 0.000000000000000000 ) ) ;
#6665=EDGE_LOOP ( 'NONE', ( #19613, #27048, #8348, #12982 ) ) ;
#6709=FACE_OUTER_BOUND ( 'NONE', #26783, .T. ) ;
#6729=ORIENTED_EDGE ( 'NONE', *, *, #16090, .T. ) ;
#6823=DIRECTION ( 'NONE',  ( -1.000000000000000000, -0.000000000000000000, -0.000000000000000000 ) ) ;
#6828=( GEOMETRIC_REPRESENTATION_CONTEXT ( 3 ) GLOBAL_UNCERTAINTY_ASSIGNED_CONTEXT ( ( #5804 ) ) GLOBAL_UNIT_ASSIGNED_CONTEXT ( ( #29293, #26475, #3783 ) ) REPRESENTATION_CONTEXT ( 'NONE', 'WORKASPACE' ) );
#7001=AXIS2_PLACEMENT_3D ( 'NONE', #20642, #32073, #36039 ) ;
#7015=CARTESIAN_POINT ( 'NONE',  ( 0.000000000000000000, 2.935248768560057453, -3.903127820947815962E-15 ) ) ;
#7126=AXIS2_PLACEMENT_3D ( 'NONE', #5604, #2804, #22862 ) ;
#7272=ORIENTED_EDGE ( 'NONE', *, *, #4576, .T. ) ;
#7430=ORIENTED_EDGE ( 'NONE', *, *, #10226, .T. ) ;
#7509=DIRECTION ( 'NONE',  ( 0.000000000000000000, 0.000000000000000000, -1.000000000000000000 ) ) ;
#7579=CARTESIAN_POINT ( 'NONE',  ( 3.000000000000000000, 0.000000000000000000, 2.541999999999999815 ) ) ;
#7676=CIRCLE ( 'NONE', #22056, 3.250000000000001332 ) ;
#7731=EDGE_CURVE ( 'NONE', #3751, #5803, #35366, .T. ) ;
#7784=ORIENTED_EDGE ( 'NONE', *, *, #36651, .F. ) ;
#7787=DIRECTION ( 'NONE',  ( 0.000000000000000000, 1.000000000000000000, -1.224646799147353207E-16 ) ) ;
#7853=CARTESIAN_POINT ( 'NONE',  ( 6.249999999999998224, 0.000000000000000000, 0.000000000000000000 ) ) ;
#7880=VERTEX_POINT ( 'NONE', #15219 ) ;
#7888=DIRECTION ( 'NONE',  ( 0.000000000000000000, -0.4999999999999990563, 0.8660254037844391517 ) ) ;
#7899=DIRECTION ( 'NONE',  ( 0.000000000000000000, 0.5000000000000013323, 0.8660254037844378194 ) ) ;
#7940=AXIS2_PLACEMENT_3D ( 'NONE', #31488, #17066, #5827 ) ;
#8036=AXIS2_PLACEMENT_3D ( 'NONE', #14818, #12554, #20605 ) ;
#8074=ORIENTED_EDGE ( 'NONE', *, *, #16870, .T. ) ;
#8075=ORIENTED_EDGE ( 'NONE', *, *, #21339, .F. ) ;
#8089=EDGE_LOOP ( 'NONE', ( #3191, #17433, #35199, #9958 ) ) ;
#8195=AXIS2_PLACEMENT_3D ( 'NONE', #4213, #18247, #10206 ) ;
#8211=CIRCLE ( 'NONE', #24379, 5.000000000000000000 ) ;
#8257=LINE ( 'NONE', #5263, #25434 ) ;
#8348=ORIENTED_EDGE ( 'NONE', *, *, #16090, .F. ) ;
#8375=FACE_OUTER_BOUND ( 'NONE', #6401, .T. ) ;
#8409=DIRECTION ( 'NONE',  ( -1.000000000000000000, -0.000000000000000000, -0.000000000000000000 ) ) ;
#8427=ORIENTED_EDGE ( 'NONE', *, *, #21645, .T. ) ;
#8431=CARTESIAN_POINT ( 'NONE',  ( 6.249999999999998224, 3.673940397442060854E-16, -3.000000000000000888 ) ) ;
#8639=FACE_OUTER_BOUND ( 'NONE', #36520, .T. ) ;
#8652=DIRECTION ( 'NONE',  ( 1.000000000000000000, 0.000000000000000000, 0.000000000000000000 ) ) ;
#8654=ORIENTED_EDGE ( 'NONE', *, *, #13180, .T. ) ;
#8714=DIRECTION ( 'NONE',  ( 0.000000000000000000, 1.000000000000000000, -1.625241993126352989E-15 ) ) ;
#8730=ORIENTED_EDGE ( 'NONE', *, *, #29066, .T. ) ;
#8764=FACE_BOUND ( 'NONE', #31766, .T. ) ;
#8785=LINE ( 'NONE', #27921, #5701 ) ;
#8832=DIRECTION ( 'NONE',  ( 0.000000000000000000, 0.000000000000000000, -1.000000000000000000 ) ) ;
#8843=CARTESIAN_POINT ( 'NONE',  ( 6.249999999999998224, 0.000000000000000000, 0.000000000000000000 ) ) ;
#8896=CARTESIAN_POINT ( 'NONE',  ( 0.000000000000000000, 0.000000000000000000, 0.000000000000000000 ) ) ;
#8984=VERTEX_POINT ( 'NONE', #20278 ) ;
#9152=FACE_OUTER_BOUND ( 'NONE', #17944, .T. ) ;
#9211=FACE_OUTER_BOUND ( 'NONE', #30486, .T. ) ;
#9219=DIRECTION ( 'NONE',  ( 1.000000000000000000, 0.000000000000000000, 0.000000000000000000 ) ) ;
#9222=CARTESIAN_POINT ( 'NONE',  ( 3.000000000000000000, 2.935248768560057453, -3.903127820947815962E-15 ) ) ;
#9352=COLOUR_RGB ( '', 0.40784314, 0.44705882, 0.49803922) ;
#9437=LINE ( 'NONE', #21049, #22018 ) ;
#9478=EDGE_CURVE ( 'NONE', #2491, #10475, #22543, .T. ) ;
#9569=VECTOR ( 'NONE', #8714, 1000.000000000000000 ) ;
#9577=EDGE_LOOP ( 'NONE', ( #31326, #2003, #8074, #15797 ) ) ;
#9578=CARTESIAN_POINT ( 'NONE',  ( 3.000000000000000000, 1.467624384280024730, -2.542000000000001592 ) ) ;
#9670=DIRECTION ( 'NONE',  ( 0.000000000000000000, 0.000000000000000000, -1.000000000000000000 ) ) ;
#9701=CARTESIAN_POINT ( 'NONE',  ( 5.999999999999998224, 0.000000000000000000, 0.000000000000000000 ) ) ;
#9885=ADVANCED_FACE ( 'NONE', ( #6393 ), #30938, .F. ) ;
#9953=AXIS2_PLACEMENT_3D ( 'NONE', #22210, #19224, #25385 ) ;
#9958=ORIENTED_EDGE ( 'NONE', *, *, #21645, .F. ) ;
#9990=EDGE_CURVE ( 'NONE', #30219, #8984, #26451, .T. ) ;
#10043=CIRCLE ( 'NONE', #19627, 0.2500000000000002220 ) ;
#10147=CARTESIAN_POINT ( 'NONE',  ( 3.000000000000000000, -2.935248768560059229, 3.469446951953614189E-15 ) ) ;
#10155=EDGE_CURVE ( 'NONE', #30219, #34090, #14041, .T. ) ;
#10162=ADVANCED_FACE ( 'NONE', ( #19501 ), #18954, .F. ) ;
#10173=DIRECTION ( 'NONE',  ( -1.000000000000000000, -0.000000000000000000, -0.000000000000000000 ) ) ;
#10206=DIRECTION ( 'NONE',  ( 0.000000000000000000, 0.000000000000000000, 1.000000000000000000 ) ) ;
#10226=EDGE_CURVE ( 'NONE', #36602, #27228, #8257, .T. ) ;
#10254=ADVANCED_FACE ( 'NONE', ( #16152 ), #28295, .T. ) ;
#10308=DIRECTION ( 'NONE',  ( -1.000000000000000000, -0.000000000000000000, -0.000000000000000000 ) ) ;
#10384=CARTESIAN_POINT ( 'NONE',  ( 0.3000000000000016542, 6.123233995736766282E-16, -5.000000000000000000 ) ) ;
#10446=ORIENTED_EDGE ( 'NONE', *, *, #36465, .F. ) ;
#10467=DIRECTION ( 'NONE',  ( -0.7071067811865288100, 0.000000000000000000, 0.7071067811865663355 ) ) ;
#10475=VERTEX_POINT ( 'NONE', #13093 ) ;
#10508=FACE_OUTER_BOUND ( 'NONE', #11277, .T. ) ;
#10567=VECTOR ( 'NONE', #24417, 1000.000000000000000 ) ;
#10650=ORIENTED_EDGE ( 'NONE', *, *, #27726, .T. ) ;
#10694=EDGE_LOOP ( 'NONE', ( #4792, #1269, #32589, #22688, #11786 ) ) ;
#10707=DIRECTION ( 'NONE',  ( 0.000000000000000000, 0.000000000000000000, 1.000000000000000000 ) ) ;
#11023=ADVANCED_FACE ( 'NONE', ( #27791 ), #31177, .F. ) ;
#11036=LINE ( 'NONE', #22479, #17681 ) ;
#11051=FACE_OUTER_BOUND ( 'NONE', #8089, .T. ) ;
#11155=PLANE ( 'NONE',  #12235 ) ;
#11195=VERTEX_POINT ( 'NONE', #25910 ) ;
#11198=CONICAL_SURFACE ( 'NONE', #7001, 2.541999999999999815, 1.047197551196591858 ) ;
#11269=AXIS2_PLACEMENT_3D ( 'NONE', #16861, #22299, #28280 ) ;
#11277=EDGE_LOOP ( 'NONE', ( #26562, #27918, #32448, #23382, #33652 ) ) ;
#11354=CARTESIAN_POINT ( 'NONE',  ( -31.74999999999995737, 0.000000000000000000, 5.000000000000000000 ) ) ;
#11460=ADVANCED_FACE ( 'NONE', ( #17054 ), #1106, .T. ) ;
#11486=EDGE_CURVE ( 'NONE', #36783, #2687, #16698, .T. ) ;
#11546=ADVANCED_FACE ( 'NONE', ( #10508 ), #548, .F. ) ;
#11550=ORIENTED_EDGE ( 'NONE', *, *, #26528, .F. ) ;
#11563=ADVANCED_FACE ( 'NONE', ( #20786 ), #5331, .T. ) ;
#11621=CARTESIAN_POINT ( 'NONE',  ( 3.000000000000000000, 2.935248768560057453, -3.903127820947815962E-15 ) ) ;
#11714=CARTESIAN_POINT ( 'NONE',  ( 3.000000000000000000, 3.113052163432572109E-16, -2.541999999999999815 ) ) ;
#11786=ORIENTED_EDGE ( 'NONE', *, *, #6461, .T. ) ;
#11790=ORIENTED_EDGE ( 'NONE', *, *, #23458, .F. ) ;
#11822=DIRECTION ( 'NONE',  ( 0.000000000000000000, 0.000000000000000000, 1.000000000000000000 ) ) ;
#11855=EDGE_CURVE ( 'NONE', #7880, #14355, #32251, .T. ) ;
#11949=EDGE_CURVE ( 'NONE', #25264, #36242, #27703, .T. ) ;
#11953=CARTESIAN_POINT ( 'NONE',  ( 5.999999999999998224, 0.000000000000000000, 5.000000000000000000 ) ) ;
#11970=FACE_BOUND ( 'NONE', #4352, .T. ) ;
#11972=DIRECTION ( 'NONE',  ( -1.000000000000000000, -0.000000000000000000, -0.000000000000000000 ) ) ;
#12111=DIRECTION ( 'NONE',  ( 0.000000000000000000, 0.000000000000000000, 1.000000000000000000 ) ) ;
#12139=ORIENTED_EDGE ( 'NONE', *, *, #9990, .T. ) ;
#12151=ORIENTED_EDGE ( 'NONE', *, *, #28504, .T. ) ;
#12157=ORIENTED_EDGE ( 'NONE', *, *, #11949, .F. ) ;
#12162=EDGE_LOOP ( 'NONE', ( #152, #27749, #30528, #6331 ) ) ;
#12167=VERTEX_POINT ( 'NONE', #15305 ) ;
#12234=ORIENTED_EDGE ( 'NONE', *, *, #34988, .F. ) ;
#12235=AXIS2_PLACEMENT_3D ( 'NONE', #2717, #23152, #28942 ) ;
#12279=VECTOR ( 'NONE', #17367, 1000.000000000000114 ) ;
#12357=EDGE_LOOP ( 'NONE', ( #6729, #15760 ) ) ;
#12409=EDGE_CURVE ( 'NONE', #17975, #26476, #16613, .T. ) ;
#12500=AXIS2_PLACEMENT_3D ( 'NONE', #33551, #13837, #16290 ) ;
#12542=ORIENTED_EDGE ( 'NONE', *, *, #627, .T. ) ;
#12554=DIRECTION ( 'NONE',  ( -1.000000000000000000, -0.000000000000000000, -0.000000000000000000 ) ) ;
#12558=CARTESIAN_POINT ( 'NONE',  ( 3.000000000000000000, 2.935248768560057453, -3.903127820947815962E-15 ) ) ;
#12858=ORIENTED_EDGE ( 'NONE', *, *, #33538, .T. ) ;
#12956=CARTESIAN_POINT ( 'NONE',  ( -31.74999999999995737, 0.000000000000000000, 0.000000000000000000 ) ) ;
#12982=ORIENTED_EDGE ( 'NONE', *, *, #11486, .F. ) ;
#13093=CARTESIAN_POINT ( 'NONE',  ( 35.99999999999999289, 3.334407072378457159E-16, -2.445500000000000007 ) ) ;
#13144=DIRECTION ( 'NONE',  ( 1.000000000000000000, 0.000000000000000000, 0.000000000000000000 ) ) ;
#13180=EDGE_CURVE ( 'NONE', #27228, #3559, #9437, .T. ) ;
#13193=ORIENTED_EDGE ( 'NONE', *, *, #32232, .F. ) ;
#13218=ADVANCED_FACE ( 'NONE', ( #33616 ), #4750, .T. ) ;
#13257=CARTESIAN_POINT ( 'NONE',  ( 0.3000000000000016542, 0.000000000000000000, 0.000000000000000000 ) ) ;
#13314=DIRECTION ( 'NONE',  ( 0.000000000000000000, -0.5000000000000013323, -0.8660254037844379305 ) ) ;
#13337=CARTESIAN_POINT ( 'NONE',  ( 3.000000000000000000, -2.935248768560059229, 3.469446951953614189E-15 ) ) ;
#13374=DIRECTION ( 'NONE',  ( -0.7071067811865288100, 8.659560562355164586E-17, -0.7071067811865663355 ) ) ;
#13408=EDGE_LOOP ( 'NONE', ( #24145, #31132, #765, #25241, #30132 ) ) ;
#13448=DIRECTION ( 'NONE',  ( 0.000000000000000000, -0.5000000000000011102, -0.8660254037844379305 ) ) ;
#13496=AXIS2_PLACEMENT_3D ( 'NONE', #19244, #34235, #31036 ) ;
#13508=LINE ( 'NONE', #19708, #401 ) ;
#13547=ORIENTED_EDGE ( 'NONE', *, *, #32717, .T. ) ;
#13670=CARTESIAN_POINT ( 'NONE',  ( 3.000000000000000000, -2.201436576420045643, -1.270999999999998575 ) ) ;
#13709=DIRECTION ( 'NONE',  ( 0.000000000000000000, -1.000000000000000000, 1.034244904716769672E-15 ) ) ;
#13832=ADVANCED_FACE ( 'NONE', ( #19861 ), #5441, .T. ) ;
#13837=DIRECTION ( 'NONE',  ( -1.000000000000000000, -0.000000000000000000, -0.000000000000000000 ) ) ;
#13855=DIRECTION ( 'NONE',  ( -1.000000000000000000, -0.000000000000000000, -0.000000000000000000 ) ) ;
#13889=CARTESIAN_POINT ( 'NONE',  ( 3.000000000000000000, -2.935248768560059229, 3.469446951953614189E-15 ) ) ;
#13999=MECHANICAL_DESIGN_GEOMETRIC_PRESENTATION_REPRESENTATION('',(#28373),#6828);
#14024=LINE ( 'NONE', #16855, #5683 ) ;
#14041=LINE ( 'NONE', #34138, #30977 ) ;
#14056=CIRCLE ( 'NONE', #20085, 5.000000000000000000 ) ;
#14061=FACE_OUTER_BOUND ( 'NONE', #17895, .T. ) ;
#14064=DIRECTION ( 'NONE',  ( -1.000000000000000000, -0.000000000000000000, -0.000000000000000000 ) ) ;
#14211=AXIS2_PLACEMENT_3D ( 'NONE', #32507, #6823, #23527 ) ;
#14310=VECTOR ( 'NONE', #13448, 1000.000000000000114 ) ;
#14355=VERTEX_POINT ( 'NONE', #29527 ) ;
#14455=ORIENTED_EDGE ( 'NONE', *, *, #23004, .F. ) ;
#14470=TOROIDAL_SURFACE ( 'NONE', #27037, 3.250000000000001332, 0.2500000000000000000 ) ;
#14471=AXIS2_PLACEMENT_3D ( 'NONE', #11621, #23075, #8832 ) ;
#14484=DIRECTION ( 'NONE',  ( -1.000000000000000000, -0.000000000000000000, -0.000000000000000000 ) ) ;
#14491=DIRECTION ( 'NONE',  ( 0.000000000000000000, 0.000000000000000000, -1.000000000000000000 ) ) ;
#14533=CARTESIAN_POINT ( 'NONE',  ( 35.99999999999999289, 0.000000000000000000, 0.000000000000000000 ) ) ;
#14584=DIRECTION ( 'NONE',  ( 0.000000000000000000, 0.000000000000000000, 1.000000000000000000 ) ) ;
#14640=CARTESIAN_POINT ( 'NONE',  ( 3.000000000000000000, 2.935248768560057453, -3.903127820947815962E-15 ) ) ;
#14792=AXIS2_PLACEMENT_3D ( 'NONE', #1485, #36182, #2432 ) ;
#14818=CARTESIAN_POINT ( 'NONE',  ( 0.000000000000000000, 0.000000000000000000, 0.000000000000000000 ) ) ;
#14901=EDGE_CURVE ( 'NONE', #19348, #22787, #36150, .T. ) ;
#14948=CARTESIAN_POINT ( 'NONE',  ( 5.999999999999998224, 0.000000000000000000, 0.000000000000000000 ) ) ;
#14991=DIRECTION ( 'NONE',  ( 0.000000000000000000, 0.000000000000000000, 1.000000000000000000 ) ) ;
#15198=ORIENTED_EDGE ( 'NONE', *, *, #19956, .T. ) ;
#15219=CARTESIAN_POINT ( 'NONE',  ( 35.44550000000001688, 3.673940397442061840E-16, -3.000000000000001776 ) ) ;
#15305=CARTESIAN_POINT ( 'NONE',  ( 0.000000000000000000, 1.467624384280024730, -2.542000000000001592 ) ) ;
#15355=VECTOR ( 'NONE', #19532, 1000.000000000000114 ) ;
#15457=LINE ( 'NONE', #7015, #22070 ) ;
#15497=CONICAL_SURFACE ( 'NONE', #36462, 2.541999999999999815, 1.047197551196591858 ) ;
#15580=EDGE_LOOP ( 'NONE', ( #22913, #23591, #16150, #3627, #10650 ) ) ;
#15590=DIRECTION ( 'NONE',  ( 0.000000000000000000, 0.000000000000000000, -1.000000000000000000 ) ) ;
#15666=CARTESIAN_POINT ( 'NONE',  ( 5.999999999999999112, 0.000000000000000000, -3.250000000000001332 ) ) ;
#15745=DIRECTION ( 'NONE',  ( -1.000000000000000000, -0.000000000000000000, -0.000000000000000000 ) ) ;
#15760=ORIENTED_EDGE ( 'NONE', *, *, #19595, .T. ) ;
#15770=ORIENTED_EDGE ( 'NONE', *, *, #16277, .T. ) ;
#15797=ORIENTED_EDGE ( 'NONE', *, *, #11855, .F. ) ;
#16090=EDGE_CURVE ( 'NONE', #2687, #11195, #3491, .T. ) ;
#16118=AXIS2_PLACEMENT_3D ( 'NONE', #451, #23147, #35153 ) ;
#16119=DIRECTION ( 'NONE',  ( -0.000000000000000000, 1.000000000000000000, 1.224646799147353207E-16 ) ) ;
#16133=EDGE_CURVE ( 'NONE', #34090, #19348, #32211, .T. ) ;
#16150=ORIENTED_EDGE ( 'NONE', *, *, #32252, .T. ) ;
#16152=FACE_OUTER_BOUND ( 'NONE', #13408, .T. ) ;
#16268=DIRECTION ( 'NONE',  ( 0.000000000000000000, 0.000000000000000000, 1.000000000000000000 ) ) ;
#16277=EDGE_CURVE ( 'NONE', #23050, #12167, #15457, .T. ) ;
#16283=DIRECTION ( 'NONE',  ( 0.000000000000000000, -1.000000000000000000, 1.034244904716769672E-15 ) ) ;
#16290=DIRECTION ( 'NONE',  ( 0.000000000000000000, 0.000000000000000000, 1.000000000000000000 ) ) ;
#16343=DIRECTION ( 'NONE',  ( 0.000000000000000000, 0.000000000000000000, 1.000000000000000000 ) ) ;
#16360=CIRCLE ( 'NONE', #30717, 2.541999999999999815 ) ;
#16370=VERTEX_POINT ( 'NONE', #18823 ) ;
#16399=CARTESIAN_POINT ( 'NONE',  ( 0.000000000000000000, 0.000000000000000000, 4.700000000000000178 ) ) ;
#16405=ORIENTED_EDGE ( 'NONE', *, *, #10155, .T. ) ;
#16456=VECTOR ( 'NONE', #35074, 1000.000000000000000 ) ;
#16464=LINE ( 'NONE', #19122, #30298 ) ;
#16536=DIRECTION ( 'NONE',  ( -1.000000000000000000, -0.000000000000000000, -0.000000000000000000 ) ) ;
#16613=LINE ( 'NONE', #2171, #9569 ) ;
#16698=CIRCLE ( 'NONE', #26859, 0.2999999999999999334 ) ;
#16721=DIRECTION ( 'NONE',  ( 0.000000000000000000, 0.000000000000000000, 1.000000000000000000 ) ) ;
#16739=DIRECTION ( 'NONE',  ( 0.000000000000000000, 0.4999999999999997224, -0.8660254037844388186 ) ) ;
#16810=LINE ( 'NONE', #28044, #31143 ) ;
#16855=CARTESIAN_POINT ( 'NONE',  ( 0.000000000000000000, 2.935248768560057453, -3.903127820947815962E-15 ) ) ;
#16861=CARTESIAN_POINT ( 'NONE',  ( 0.000000000000000000, 0.000000000000000000, 0.000000000000000000 ) ) ;
#16864=CARTESIAN_POINT ( 'NONE',  ( 3.000000000000000000, 2.935248768560057453, -3.903127820947815962E-15 ) ) ;
#16870=EDGE_CURVE ( 'NONE', #2491, #14355, #16464, .T. ) ;
#16875=DIRECTION ( 'NONE',  ( 0.000000000000000000, -0.5000000000000011102, -0.8660254037844379305 ) ) ;
#16918=DIRECTION ( 'NONE',  ( 1.000000000000000000, 0.000000000000000000, 0.000000000000000000 ) ) ;
#16920=EDGE_LOOP ( 'NONE', ( #8075, #17496, #36070, #21537 ) ) ;
#16926=ORIENTED_EDGE ( 'NONE', *, *, #32252, .F. ) ;
#16966=FACE_OUTER_BOUND ( 'NONE', #27619, .T. ) ;
#17054=FACE_OUTER_BOUND ( 'NONE', #35687, .T. ) ;
#17066=DIRECTION ( 'NONE',  ( 1.000000000000000000, 0.000000000000000000, 0.000000000000000000 ) ) ;
#17270=PLANE ( 'NONE',  #7940 ) ;
#17321=APPLICATION_CONTEXT ( 'automotive_design' ) ;
#17367=DIRECTION ( 'NONE',  ( -0.5000000000000051070, 1.060575238724903217E-16, -0.8660254037844355990 ) ) ;
#17409=DIRECTION ( 'NONE',  ( -1.000000000000000000, -0.000000000000000000, -0.000000000000000000 ) ) ;
#17433=ORIENTED_EDGE ( 'NONE', *, *, #34840, .T. ) ;
#17496=ORIENTED_EDGE ( 'NONE', *, *, #34112, .T. ) ;
#17580=DIRECTION ( 'NONE',  ( -1.000000000000000000, -0.000000000000000000, -0.000000000000000000 ) ) ;
#17646=EDGE_CURVE ( 'NONE', #10475, #2491, #33982, .T. ) ;
#17681=VECTOR ( 'NONE', #2992, 1000.000000000000114 ) ;
#17771=CARTESIAN_POINT ( 'NONE',  ( -31.74999999999995737, 0.000000000000000000, 0.000000000000000000 ) ) ;
#17845=DIRECTION ( 'NONE',  ( 0.000000000000000000, -1.224646799147353207E-16, 1.000000000000000000 ) ) ;
#17895=EDGE_LOOP ( 'NONE', ( #22515, #24359, #18623 ) ) ;
#17942=EDGE_CURVE ( 'NONE', #34090, #35050, #18036, .T. ) ;
#17944=EDGE_LOOP ( 'NONE', ( #10446, #2898 ) ) ;
#17975=VERTEX_POINT ( 'NONE', #32283 ) ;
#17984=DIRECTION ( 'NONE',  ( 1.000000000000000000, 0.000000000000000000, 0.000000000000000000 ) ) ;
#18012=LINE ( 'NONE', #9578, #16456 ) ;
#18036=LINE ( 'NONE', #35313, #19897 ) ;
#18095=DIRECTION ( 'NONE',  ( 0.000000000000000000, 0.000000000000000000, 1.000000000000000000 ) ) ;
#18153=( NAMED_UNIT ( * ) PLANE_ANGLE_UNIT ( ) SI_UNIT ( $, .RADIAN. ) );
#18198=COLOUR_RGB ( '', 0.40784314, 0.44705882, 0.49803922) ;
#18247=DIRECTION ( 'NONE',  ( -1.000000000000000000, -0.000000000000000000, -0.000000000000000000 ) ) ;
#18303=LINE ( 'NONE', #24303, #33278 ) ;
#18337=EDGE_CURVE ( 'NONE', #36783, #19009, #1345, .T. ) ;
#18348=( LENGTH_UNIT ( ) NAMED_UNIT ( * ) SI_UNIT ( .MILLI., .METRE. ) );
#18352=ADVANCED_FACE ( 'NONE', ( #14061 ), #17270, .F. ) ;
#18403=AXIS2_PLACEMENT_3D ( 'NONE', #8843, #8652, #202 ) ;
#18419=CARTESIAN_POINT ( 'NONE',  ( -31.74999999999995737, 6.123233995736766282E-16, -5.000000000000000000 ) ) ;
#18425=SURFACE_STYLE_USAGE ( .BOTH. , #4179 ) ;
#18430=VECTOR ( 'NONE', #6472, 1000.000000000000000 ) ;
#18623=ORIENTED_EDGE ( 'NONE', *, *, #16133, .F. ) ;
#18633=EDGE_LOOP ( 'NONE', ( #16926, #31071, #12234 ) ) ;
#18823=CARTESIAN_POINT ( 'NONE',  ( 5.999999999999998224, 6.123233995736766282E-16, -5.000000000000000000 ) ) ;
#18834=CARTESIAN_POINT ( 'NONE',  ( 0.000000000000000000, -2.935248768560059229, 3.469446951953614189E-15 ) ) ;
#18835=AXIS2_PLACEMENT_3D ( 'NONE', #28298, #30930, #10707 ) ;
#18954=PLANE ( 'NONE',  #24403 ) ;
#18981=EDGE_CURVE ( 'NONE', #10475, #7880, #24654, .T. ) ;
#19009=VERTEX_POINT ( 'NONE', #10384 ) ;
#19027=EDGE_CURVE ( 'NONE', #31926, #26476, #2512, .T. ) ;
#19040=CIRCLE ( 'NONE', #1654, 0.2999999999999999334 ) ;
#19096=VECTOR ( 'NONE', #22413, 1000.000000000000000 ) ;
#19122=CARTESIAN_POINT ( 'NONE',  ( 35.99999999999999289, 0.000000000000000000, 2.445500000000000007 ) ) ;
#19224=DIRECTION ( 'NONE',  ( -1.000000000000000000, -0.000000000000000000, -0.000000000000000000 ) ) ;
#19244=CARTESIAN_POINT ( 'NONE',  ( 3.000000000000000000, 0.000000000000000000, 0.000000000000000000 ) ) ;
#19278=MANIFOLD_SOLID_BREP ( 'Hex', #32750 ) ;
#19348=VERTEX_POINT ( 'NONE', #4740 ) ;
#19465=CIRCLE ( 'NONE', #36834, 3.000000000000000888 ) ;
#19501=FACE_OUTER_BOUND ( 'NONE', #10694, .T. ) ;
#19503=( LENGTH_UNIT ( ) NAMED_UNIT ( * ) SI_UNIT ( .MILLI., .METRE. ) );
#19505=CYLINDRICAL_SURFACE ( 'NONE', #18835, 3.000000000000000888 ) ;
#19532=DIRECTION ( 'NONE',  ( 0.000000000000000000, 0.4999999999999991118, -0.8660254037844391517 ) ) ;
#19595=EDGE_CURVE ( 'NONE', #11195, #2687, #23608, .T. ) ;
#19613=ORIENTED_EDGE ( 'NONE', *, *, #627, .F. ) ;
#19627=AXIS2_PLACEMENT_3D ( 'NONE', #24276, #7787, #29910 ) ;
#19646=AXIS2_PLACEMENT_3D ( 'NONE', #3318, #31633, #28815 ) ;
#19708=CARTESIAN_POINT ( 'NONE',  ( 0.000000000000000000, 1.467624384280024730, -2.542000000000001592 ) ) ;
#19714=LINE ( 'NONE', #13889, #36209 ) ;
#19842=ORIENTED_EDGE ( 'NONE', *, *, #33538, .F. ) ;
#19861=FACE_OUTER_BOUND ( 'NONE', #15580, .T. ) ;
#19874=DIRECTION ( 'NONE',  ( 0.000000000000000000, -1.000000000000000000, 0.000000000000000000 ) ) ;
#19897=VECTOR ( 'NONE', #29285, 1000.000000000000000 ) ;
#19956=EDGE_CURVE ( 'NONE', #23050, #29314, #14024, .T. ) ;
#20039=EDGE_LOOP ( 'NONE', ( #15770, #7784, #34494, #21523, #27868 ) ) ;
#20085=AXIS2_PLACEMENT_3D ( 'NONE', #14948, #26379, #685 ) ;
#20105=LINE ( 'NONE', #31533, #33346 ) ;
#20119=ADVANCED_FACE ( 'NONE', ( #16966 ), #11155, .F. ) ;
#20147=PRODUCT_DEFINITION_FORMATION_WITH_SPECIFIED_SOURCE ( 'ANY', '', #37010, .NOT_KNOWN. ) ;
#20205=FACE_OUTER_BOUND ( 'NONE', #12357, .T. ) ;
#20235=AXIS2_PLACEMENT_3D ( 'NONE', #31109, #13855, #31454 ) ;
#20267=CARTESIAN_POINT ( 'NONE',  ( 3.000000000000000000, 2.935248768560057453, -3.903127820947815962E-15 ) ) ;
#20272=AXIS2_PLACEMENT_3D ( 'NONE', #26419, #724, #6552 ) ;
#20273=CARTESIAN_POINT ( 'NONE',  ( -31.74999999999995737, 3.673940397442060854E-16, -3.000000000000000888 ) ) ;
#20278=CARTESIAN_POINT ( 'NONE',  ( 3.000000000000000000, 2.201436576420042535, 1.270999999999998353 ) ) ;
#20382=DIRECTION ( 'NONE',  ( -1.000000000000000000, -0.000000000000000000, -0.000000000000000000 ) ) ;
#20521=ORIENTED_EDGE ( 'NONE', *, *, #14901, .T. ) ;
#20580=PRESENTATION_STYLE_ASSIGNMENT (( #29774 ) ) ;
#20582=DIRECTION ( 'NONE',  ( 0.000000000000000000, 0.000000000000000000, -1.000000000000000000 ) ) ;
#20605=DIRECTION ( 'NONE',  ( 0.000000000000000000, 0.000000000000000000, 1.000000000000000000 ) ) ;
#20622=AXIS2_PLACEMENT_3D ( 'NONE', #27580, #36196, #7888 ) ;
#20642=CARTESIAN_POINT ( 'NONE',  ( 3.000000000000000000, 0.000000000000000000, 0.000000000000000000 ) ) ;
#20653=FILL_AREA_STYLE ('',( #21415 ) ) ;
#20654=EDGE_LOOP ( 'NONE', ( #28075, #30711, #8427, #26008 ) ) ;
#20709=LINE ( 'NONE', #11714, #12279 ) ;
#20773=AXIS2_PLACEMENT_3D ( 'NONE', #24775, #30942, #7899 ) ;
#20786=FACE_OUTER_BOUND ( 'NONE', #9577, .T. ) ;
#20839=ORIENTED_EDGE ( 'NONE', *, *, #19027, .F. ) ;
#20895=ADVANCED_FACE ( 'NONE', ( #11051 ), #19505, .T. ) ;
#21049=CARTESIAN_POINT ( 'NONE',  ( 0.000000000000000000, -2.935248768560059229, 3.469446951953614189E-15 ) ) ;
#21081=ADVANCED_FACE ( 'NONE', ( #11970, #9152 ), #25867, .T. ) ;
#21220=AXIS2_PLACEMENT_3D ( 'NONE', #6550, #17984, #20582 ) ;
#21339=EDGE_CURVE ( 'NONE', #5803, #3751, #19465, .T. ) ;
#21385=AXIS2_PLACEMENT_3D ( 'NONE', #8896, #30384, #36396 ) ;
#21415=FILL_AREA_STYLE_COLOUR ( '', #18198 ) ;
#21523=ORIENTED_EDGE ( 'NONE', *, *, #10155, .F. ) ;
#21537=ORIENTED_EDGE ( 'NONE', *, *, #24552, .F. ) ;
#21594=CARTESIAN_POINT ( 'NONE',  ( 3.000000000000000000, 2.935248768560057453, -3.903127820947815962E-15 ) ) ;
#21645=EDGE_CURVE ( 'NONE', #14355, #5803, #18303, .T. ) ;
#21908=CARTESIAN_POINT ( 'NONE',  ( 0.3000000000000016542, 5.755839955992559655E-16, -4.700000000000000178 ) ) ;
#22018=VECTOR ( 'NONE', #3631, 1000.000000000000114 ) ;
#22049=ADVANCED_FACE ( 'NONE', ( #27239 ), #14470, .F. ) ;
#22056=AXIS2_PLACEMENT_3D ( 'NONE', #32714, #29912, #9670 ) ;
#22070=VECTOR ( 'NONE', #1015, 1000.000000000000000 ) ;
#22074=TOROIDAL_SURFACE ( 'NONE', #23238, 4.700000000000000178, 0.2999999999999999889 ) ;
#22078=EDGE_LOOP ( 'NONE', ( #20839, #13547, #12151, #5389, #6423 ) ) ;
#22121=VECTOR ( 'NONE', #16283, 1000.000000000000000 ) ;
#22173=CYLINDRICAL_SURFACE ( 'NONE', #22397, 5.000000000000000000 ) ;
#22210=CARTESIAN_POINT ( 'NONE',  ( 6.000000000000000000, 0.000000000000000000, 0.000000000000000000 ) ) ;
#22299=DIRECTION ( 'NONE',  ( -1.000000000000000000, -0.000000000000000000, -0.000000000000000000 ) ) ;
#22397=AXIS2_PLACEMENT_3D ( 'NONE', #1232, #16536, #18095 ) ;
#22413=DIRECTION ( 'NONE',  ( -1.000000000000000000, -0.000000000000000000, -0.000000000000000000 ) ) ;
#22415=DIRECTION ( 'NONE',  ( 0.000000000000000000, 0.000000000000000000, 1.000000000000000000 ) ) ;
#22448=EDGE_CURVE ( 'NONE', #19009, #11195, #19040, .T. ) ;
#22479=CARTESIAN_POINT ( 'NONE',  ( 3.000000000000000000, -1.467624384280027172, 2.542000000000001592 ) ) ;
#22515=ORIENTED_EDGE ( 'NONE', *, *, #17942, .T. ) ;
#22543=CIRCLE ( 'NONE', #3378, 2.445500000000000007 ) ;
#22618=CARTESIAN_POINT ( 'NONE',  ( 0.000000000000000000, -1.467624384280027172, 2.542000000000001592 ) ) ;
#22624=EDGE_LOOP ( 'NONE', ( #26754, #19842, #33488 ) ) ;
#22662=AXIS2_PLACEMENT_3D ( 'NONE', #33396, #25319, #30933 ) ;
#22688=ORIENTED_EDGE ( 'NONE', *, *, #12409, .F. ) ;
#22738=SHAPE_REPRESENTATION ( 'socket head cap screw_iso_ISO 4762 M6 x 30 - 30N', ( #21385 ), #2159 ) ;
#22787=VERTEX_POINT ( 'NONE', #31801 ) ;
#22819=ADVANCED_FACE ( 'NONE', ( #8764, #20205 ), #6133, .T. ) ;
#22862=DIRECTION ( 'NONE',  ( 0.000000000000000000, 0.5000000000000011102, 0.8660254037844379305 ) ) ;
#22886=DIRECTION ( 'NONE',  ( 1.000000000000000000, 0.000000000000000000, 0.000000000000000000 ) ) ;
#22913=ORIENTED_EDGE ( 'NONE', *, *, #10226, .F. ) ;
#23004=EDGE_CURVE ( 'NONE', #31031, #36783, #30668, .T. ) ;
#23050=VERTEX_POINT ( 'NONE', #25619 ) ;
#23075=DIRECTION ( 'NONE',  ( 1.000000000000000000, 0.000000000000000000, 0.000000000000000000 ) ) ;
#23147=DIRECTION ( 'NONE',  ( 0.000000000000000000, -1.000000000000000000, 0.000000000000000000 ) ) ;
#23152=DIRECTION ( 'NONE',  ( 1.000000000000000000, 0.000000000000000000, 0.000000000000000000 ) ) ;
#23199=VECTOR ( 'NONE', #5502, 1000.000000000000114 ) ;
#23203=DIRECTION ( 'NONE',  ( 0.000000000000000000, 0.000000000000000000, 1.000000000000000000 ) ) ;
#23238=AXIS2_PLACEMENT_3D ( 'NONE', #5580, #8409, #34104 ) ;
#23266=LINE ( 'NONE', #20267, #35157 ) ;
#23382=ORIENTED_EDGE ( 'NONE', *, *, #31954, .F. ) ;
#23458=EDGE_CURVE ( 'NONE', #29705, #22787, #24825, .T. ) ;
#23527=DIRECTION ( 'NONE',  ( 0.000000000000000000, 0.000000000000000000, 1.000000000000000000 ) ) ;
#23591=ORIENTED_EDGE ( 'NONE', *, *, #6461, .F. ) ;
#23608=CIRCLE ( 'NONE', #8036, 4.700000000000000178 ) ;
#23628=ORIENTED_EDGE ( 'NONE', *, *, #18981, .T. ) ;
#23930=VECTOR ( 'NONE', #27937, 1000.000000000000000 ) ;
#24145=ORIENTED_EDGE ( 'NONE', *, *, #13180, .F. ) ;
#24235=AXIS2_PLACEMENT_3D ( 'NONE', #14533, #36678, #22415 ) ;
#24276=CARTESIAN_POINT ( 'NONE',  ( 6.249999999999998224, 3.980102097228899218E-16, 3.250000000000001332 ) ) ;
#24303=CARTESIAN_POINT ( 'NONE',  ( -31.74999999999995737, 0.000000000000000000, 3.000000000000000888 ) ) ;
#24358=CIRCLE ( 'NONE', #8195, 3.000000000000001332 ) ;
#24359=ORIENTED_EDGE ( 'NONE', *, *, #31954, .T. ) ;
#24379=AXIS2_PLACEMENT_3D ( 'NONE', #13257, #30520, #16268 ) ;
#24403=AXIS2_PLACEMENT_3D ( 'NONE', #33390, #5449, #30381 ) ;
#24417=DIRECTION ( 'NONE',  ( -1.000000000000000000, -0.000000000000000000, -0.000000000000000000 ) ) ;
#24518=ORIENTED_EDGE ( 'NONE', *, *, #18337, .T. ) ;
#24552=EDGE_CURVE ( 'NONE', #3751, #34152, #31643, .T. ) ;
#24654=LINE ( 'NONE', #1945, #30138 ) ;
#24775=CARTESIAN_POINT ( 'NONE',  ( 3.000000000000000000, 2.935248768560057453, -3.903127820947815962E-15 ) ) ;
#24788=ORIENTED_EDGE ( 'NONE', *, *, #36465, .T. ) ;
#24825=LINE ( 'NONE', #36806, #23199 ) ;
#24919=ORIENTED_EDGE ( 'NONE', *, *, #19595, .F. ) ;
#24930=CIRCLE ( 'NONE', #9953, 3.250000000000001332 ) ;
#24947=UNCERTAINTY_MEASURE_WITH_UNIT (LENGTH_MEASURE( 1.000000000000000082E-05 ), #19503, 'distance_accuracy_value', 'NONE');
#25081=CARTESIAN_POINT ( 'NONE',  ( 3.000000000000000000, 1.467624384280024730, -2.542000000000001592 ) ) ;
#25087=AXIS2_PLACEMENT_3D ( 'NONE', #346, #11972, #14991 ) ;
#25141=CARTESIAN_POINT ( 'NONE',  ( 0.000000000000000000, -1.467624384280032501, -2.541999999999998483 ) ) ;
#25241=ORIENTED_EDGE ( 'NONE', *, *, #23458, .T. ) ;
#25264=VERTEX_POINT ( 'NONE', #5413 ) ;
#25302=AXIS2_PLACEMENT_3D ( 'NONE', #21594, #13144, #15590 ) ;
#25319=DIRECTION ( 'NONE',  ( -1.000000000000000000, -0.000000000000000000, -0.000000000000000000 ) ) ;
#25340=CARTESIAN_POINT ( 'NONE',  ( 3.000000000000000000, 1.467624384280029615, 2.541999999999997151 ) ) ;
#25374=EDGE_CURVE ( 'NONE', #26476, #8984, #5994, .T. ) ;
#25385=DIRECTION ( 'NONE',  ( 0.000000000000000000, 0.000000000000000000, -1.000000000000000000 ) ) ;
#25434=VECTOR ( 'NONE', #16875, 1000.000000000000114 ) ;
#25483=FACE_OUTER_BOUND ( 'NONE', #22624, .T. ) ;
#25619=CARTESIAN_POINT ( 'NONE',  ( 0.000000000000000000, 2.935248768560057453, -3.903127820947815962E-15 ) ) ;
#25638=EDGE_CURVE ( 'NONE', #26476, #30547, #16810, .T. ) ;
#25867=PLANE ( 'NONE',  #21220 ) ;
#25893=PLANE ( 'NONE',  #14471 ) ;
#25910=CARTESIAN_POINT ( 'NONE',  ( 0.000000000000000000, 5.939536975864662969E-16, -4.700000000000000178 ) ) ;
#25928=PRODUCT_DEFINITION_SHAPE ( 'NONE', 'NONE',  #1995 ) ;
#26008=ORIENTED_EDGE ( 'NONE', *, *, #21339, .T. ) ;
#26010=ORIENTED_EDGE ( 'NONE', *, *, #32983, .T. ) ;
#26046=ORIENTED_EDGE ( 'NONE', *, *, #16277, .F. ) ;
#26080=DIRECTION ( 'NONE',  ( -1.000000000000000000, -0.000000000000000000, -0.000000000000000000 ) ) ;
#26084=DIRECTION ( 'NONE',  ( 0.000000000000000000, -0.4999999999999996114, 0.8660254037844388186 ) ) ;
#26159=VECTOR ( 'NONE', #26084, 1000.000000000000000 ) ;
#26163=EDGE_CURVE ( 'NONE', #22787, #3559, #20105, .T. ) ;
#26261=ADVANCED_FACE ( 'NONE', ( #9211 ), #11198, .F. ) ;
#26328=DIRECTION ( 'NONE',  ( 0.000000000000000000, 0.000000000000000000, 1.000000000000000000 ) ) ;
#26379=DIRECTION ( 'NONE',  ( -1.000000000000000000, -0.000000000000000000, -0.000000000000000000 ) ) ;
#26380=SHAPE_DEFINITION_REPRESENTATION ( #25928, #22738 ) ;
#26407=CYLINDRICAL_SURFACE ( 'NONE', #2699, 5.000000000000000000 ) ;
#26419=CARTESIAN_POINT ( 'NONE',  ( 3.000000000000000000, 1.467624384280024730, -2.542000000000001592 ) ) ;
#26451=LINE ( 'NONE', #14640, #26159 ) ;
#26463=ADVANCED_FACE ( 'NONE', ( #5624 ), #5076, .F. ) ;
#26475=( NAMED_UNIT ( * ) PLANE_ANGLE_UNIT ( ) SI_UNIT ( $, .RADIAN. ) );
#26476=VERTEX_POINT ( 'NONE', #33960 ) ;
#26528=EDGE_CURVE ( 'NONE', #12167, #3559, #13508, .T. ) ;
#26562=ORIENTED_EDGE ( 'NONE', *, *, #26528, .T. ) ;
#26754=ORIENTED_EDGE ( 'NONE', *, *, #25638, .T. ) ;
#26783=EDGE_LOOP ( 'NONE', ( #24788, #8730, #12542, #14455 ) ) ;
#26819=LINE ( 'NONE', #12558, #30963 ) ;
#26859=AXIS2_PLACEMENT_3D ( 'NONE', #36947, #19874, #5070 ) ;
#26917=FACE_OUTER_BOUND ( 'NONE', #30753, .T. ) ;
#27000=ADVANCED_FACE ( 'NONE', ( #8375 ), #2101, .T. ) ;
#27014=DIRECTION ( 'NONE',  ( 1.000000000000000000, 0.000000000000000000, 0.000000000000000000 ) ) ;
#27037=AXIS2_PLACEMENT_3D ( 'NONE', #4574, #30060, #27062 ) ;
#27048=ORIENTED_EDGE ( 'NONE', *, *, #22448, .T. ) ;
#27062=DIRECTION ( 'NONE',  ( 0.000000000000000000, 0.000000000000000000, -1.000000000000000000 ) ) ;
#27228=VERTEX_POINT ( 'NONE', #18834 ) ;
#27239=FACE_OUTER_BOUND ( 'NONE', #16920, .T. ) ;
#27390=CARTESIAN_POINT ( 'NONE',  ( 36.00000000000000000, 2.445500000000000007, 0.000000000000000000 ) ) ;
#27406=LINE ( 'NONE', #18419, #10567 ) ;
#27422=CARTESIAN_POINT ( 'NONE',  ( 3.000000000000000000, 2.935248768560057453, -3.903127820947815962E-15 ) ) ;
#27565=AXIS2_PLACEMENT_3D ( 'NONE', #35002, #20382, #23203 ) ;
#27580=CARTESIAN_POINT ( 'NONE',  ( 3.000000000000000000, -2.935248768560059229, 3.469446951953614189E-15 ) ) ;
#27619=EDGE_LOOP ( 'NONE', ( #32923, #16405, #4767 ) ) ;
#27675=DIRECTION ( 'NONE',  ( 0.000000000000000000, 0.000000000000000000, 1.000000000000000000 ) ) ;
#27703=LINE ( 'NONE', #2021, #14310 ) ;
#27726=EDGE_CURVE ( 'NONE', #36242, #27228, #19714, .T. ) ;
#27749=ORIENTED_EDGE ( 'NONE', *, *, #7731, .F. ) ;
#27760=CYLINDRICAL_SURFACE ( 'NONE', #345, 3.000000000000000888 ) ;
#27791=FACE_OUTER_BOUND ( 'NONE', #29236, .T. ) ;
#27868=ORIENTED_EDGE ( 'NONE', *, *, #33728, .T. ) ;
#27918=ORIENTED_EDGE ( 'NONE', *, *, #26163, .F. ) ;
#27921=CARTESIAN_POINT ( 'NONE',  ( 0.000000000000000000, -1.467624384280027172, 2.542000000000001592 ) ) ;
#27937=DIRECTION ( 'NONE',  ( -1.000000000000000000, -0.000000000000000000, -0.000000000000000000 ) ) ;
#27979=ORIENTED_EDGE ( 'NONE', *, *, #5240, .F. ) ;
#28044=CARTESIAN_POINT ( 'NONE',  ( 3.000000000000000000, -1.467624384280027172, 2.542000000000001592 ) ) ;
#28060=ORIENTED_EDGE ( 'NONE', *, *, #28312, .T. ) ;
#28075=ORIENTED_EDGE ( 'NONE', *, *, #34840, .F. ) ;
#28091=CARTESIAN_POINT ( 'NONE',  ( 6.249999999999998224, 0.000000000000000000, 3.000000000000000888 ) ) ;
#28108=FACE_OUTER_BOUND ( 'NONE', #22078, .T. ) ;
#28276=DIRECTION ( 'NONE',  ( 0.000000000000000000, -0.4999999999999996114, 0.8660254037844388186 ) ) ;
#28280=DIRECTION ( 'NONE',  ( 0.000000000000000000, 0.000000000000000000, 1.000000000000000000 ) ) ;
#28295=PLANE ( 'NONE',  #20622 ) ;
#28298=CARTESIAN_POINT ( 'NONE',  ( -31.74999999999995737, 0.000000000000000000, 0.000000000000000000 ) ) ;
#28301=ORIENTED_EDGE ( 'NONE', *, *, #29066, .F. ) ;
#28312=EDGE_CURVE ( 'NONE', #16370, #31031, #14056, .T. ) ;
#28373=STYLED_ITEM ( 'NONE', ( #29851 ), #19278 ) ;
#28481=LINE ( 'NONE', #36751, #23930 ) ;
#28504=EDGE_CURVE ( 'NONE', #19348, #29705, #36269, .T. ) ;
#28534=CARTESIAN_POINT ( 'NONE',  ( 3.000000000000000000, 2.935248768560057453, -3.903127820947815962E-15 ) ) ;
#28815=DIRECTION ( 'NONE',  ( -0.000000000000000000, 0.000000000000000000, 1.000000000000000000 ) ) ;
#28942=DIRECTION ( 'NONE',  ( 0.000000000000000000, 0.000000000000000000, -1.000000000000000000 ) ) ;
#29066=EDGE_CURVE ( 'NONE', #16370, #19009, #27406, .T. ) ;
#29204=ADVANCED_FACE ( 'NONE', ( #4909 ), #27760, .T. ) ;
#29236=EDGE_LOOP ( 'NONE', ( #20521, #11790, #35739 ) ) ;
#29285=DIRECTION ( 'NONE',  ( 0.000000000000000000, -0.5000000000000013323, -0.8660254037844379305 ) ) ;
#29293=( LENGTH_UNIT ( ) NAMED_UNIT ( * ) SI_UNIT ( .MILLI., .METRE. ) );
#29314=VERTEX_POINT ( 'NONE', #31146 ) ;
#29407=FILL_AREA_STYLE_COLOUR ( '', #9352 ) ;
#29527=CARTESIAN_POINT ( 'NONE',  ( 35.44550000000001688, 0.000000000000000000, 3.000000000000001332 ) ) ;
#29705=VERTEX_POINT ( 'NONE', #13670 ) ;
#29774=SURFACE_STYLE_USAGE ( .BOTH. , #35249 ) ;
#29789=AXIS2_PLACEMENT_3D ( 'NONE', #27422, #30420, #16739 ) ;
#29851=PRESENTATION_STYLE_ASSIGNMENT (( #18425 ) ) ;
#29910=DIRECTION ( 'NONE',  ( 0.000000000000000000, 1.224646799147351482E-16, 1.000000000000000000 ) ) ;
#29912=DIRECTION ( 'NONE',  ( -1.000000000000000000, -0.000000000000000000, -0.000000000000000000 ) ) ;
#30060=DIRECTION ( 'NONE',  ( 1.000000000000000000, 0.000000000000000000, 0.000000000000000000 ) ) ;
#30132=ORIENTED_EDGE ( 'NONE', *, *, #26163, .T. ) ;
#30138=VECTOR ( 'NONE', #13374, 999.9999999999998863 ) ;
#30178=UNCERTAINTY_MEASURE_WITH_UNIT (LENGTH_MEASURE( 1.000000000000000082E-05 ), #18348, 'distance_accuracy_value', 'NONE');
#30219=VERTEX_POINT ( 'NONE', #9222 ) ;
#30230=AXIS2_PLACEMENT_3D ( 'NONE', #16864, #2800, #5600 ) ;
#30262=ORIENTED_EDGE ( 'NONE', *, *, #22448, .F. ) ;
#30298=VECTOR ( 'NONE', #10467, 999.9999999999998863 ) ;
#30381=DIRECTION ( 'NONE',  ( 0.000000000000000000, -1.000000000000000000, 1.625241993126352989E-15 ) ) ;
#30384=DIRECTION ( 'NONE',  ( 0.000000000000000000, 0.000000000000000000, 1.000000000000000000 ) ) ;
#30385=FACE_OUTER_BOUND ( 'NONE', #18633, .T. ) ;
#30420=DIRECTION ( 'NONE',  ( 0.000000000000000000, -0.8660254037844388186, -0.4999999999999997224 ) ) ;
#30486=EDGE_LOOP ( 'NONE', ( #37073, #1363, #34653, #7272, #32579 ) ) ;
#30508=DIRECTION ( 'NONE',  ( -1.000000000000000000, -0.000000000000000000, -0.000000000000000000 ) ) ;
#30520=DIRECTION ( 'NONE',  ( 1.000000000000000000, 0.000000000000000000, 0.000000000000000000 ) ) ;
#30528=ORIENTED_EDGE ( 'NONE', *, *, #24552, .T. ) ;
#30547=VERTEX_POINT ( 'NONE', #25340 ) ;
#30549=AXIS2_PLACEMENT_3D ( 'NONE', #32288, #9219, #14491 ) ;
#30581=PLANE ( 'NONE',  #25302 ) ;
#30668=LINE ( 'NONE', #11354, #19096 ) ;
#30707=FACE_OUTER_BOUND ( 'NONE', #6665, .T. ) ;
#30711=ORIENTED_EDGE ( 'NONE', *, *, #11855, .T. ) ;
#30717=AXIS2_PLACEMENT_3D ( 'NONE', #36016, #10308, #32438 ) ;
#30753=EDGE_LOOP ( 'NONE', ( #28301, #28060, #2558, #24518 ) ) ;
#30874=AXIS2_PLACEMENT_3D ( 'NONE', #388, #26080, #11822 ) ;
#30898=( GEOMETRIC_REPRESENTATION_CONTEXT ( 3 ) GLOBAL_UNCERTAINTY_ASSIGNED_CONTEXT ( ( #30178 ) ) GLOBAL_UNIT_ASSIGNED_CONTEXT ( ( #18348, #18153, #3902 ) ) REPRESENTATION_CONTEXT ( 'NONE', 'WORKASPACE' ) );
#30919=PRODUCT_DEFINITION_CONTEXT ( 'detailed design', #30999, 'design' ) ;
#30930=DIRECTION ( 'NONE',  ( -1.000000000000000000, -0.000000000000000000, -0.000000000000000000 ) ) ;
#30933=DIRECTION ( 'NONE',  ( 0.000000000000000000, 0.000000000000000000, 1.000000000000000000 ) ) ;
#30938=TOROIDAL_SURFACE ( 'NONE', #18403, 3.250000000000001332, 0.2500000000000000000 ) ;
#30942=DIRECTION ( 'NONE',  ( 0.000000000000000000, 0.8660254037844379305, -0.5000000000000014433 ) ) ;
#30959=LINE ( 'NONE', #13337, #15355 ) ;
#30963=VECTOR ( 'NONE', #15745, 1000.000000000000000 ) ;
#30977=VECTOR ( 'NONE', #13314, 1000.000000000000000 ) ;
#30992=STYLED_ITEM ( 'NONE', ( #20580 ), #4968 ) ;
#30999=APPLICATION_CONTEXT ( 'automotive_design' ) ;
#31016=ADVANCED_FACE ( 'NONE', ( #28108 ), #15497, .F. ) ;
#31031=VERTEX_POINT ( 'NONE', #11953 ) ;
#31036=DIRECTION ( 'NONE',  ( 0.000000000000000000, 0.000000000000000000, 1.000000000000000000 ) ) ;
#31056=LINE ( 'NONE', #25081, #1013 ) ;
#31071=ORIENTED_EDGE ( 'NONE', *, *, #12409, .T. ) ;
#31109=CARTESIAN_POINT ( 'NONE',  ( 3.000000000000000000, 0.000000000000000000, 0.000000000000000000 ) ) ;
#31132=ORIENTED_EDGE ( 'NONE', *, *, #27726, .F. ) ;
#31143=VECTOR ( 'NONE', #2170, 1000.000000000000000 ) ;
#31146=CARTESIAN_POINT ( 'NONE',  ( 0.000000000000000000, 1.467624384280029615, 2.541999999999997151 ) ) ;
#31177=PLANE ( 'NONE',  #37012 ) ;
#31326=ORIENTED_EDGE ( 'NONE', *, *, #18981, .F. ) ;
#31371=EDGE_LOOP ( 'NONE', ( #33234, #32202 ) ) ;
#31454=DIRECTION ( 'NONE',  ( 0.000000000000000000, 0.000000000000000000, 1.000000000000000000 ) ) ;
#31488=CARTESIAN_POINT ( 'NONE',  ( 3.000000000000000000, 2.935248768560057453, -3.903127820947815962E-15 ) ) ;
#31533=CARTESIAN_POINT ( 'NONE',  ( 3.000000000000000000, -1.467624384280032501, -2.541999999999998483 ) ) ;
#31612=ADVANCED_FACE ( 'NONE', ( #26917 ), #22173, .T. ) ;
#31633=DIRECTION ( 'NONE',  ( -1.000000000000000000, 0.000000000000000000, -0.000000000000000000 ) ) ;
#31643=CIRCLE ( 'NONE', #16118, 0.2500000000000002220 ) ;
#31697=DIRECTION ( 'NONE',  ( -1.000000000000000000, -0.000000000000000000, -0.000000000000000000 ) ) ;
#31766=EDGE_LOOP ( 'NONE', ( #15198, #13193, #7430, #8654, #11550, #26046 ) ) ;
#31801=CARTESIAN_POINT ( 'NONE',  ( 3.000000000000000000, -1.467624384280032501, -2.541999999999998483 ) ) ;
#31805=ORIENTED_EDGE ( 'NONE', *, *, #18337, .F. ) ;
#31926=VERTEX_POINT ( 'NONE', #1136 ) ;
#31954=EDGE_CURVE ( 'NONE', #35050, #19348, #18012, .T. ) ;
#31978=ORIENTED_EDGE ( 'NONE', *, *, #11486, .T. ) ;
#32073=DIRECTION ( 'NONE',  ( -1.000000000000000000, -0.000000000000000000, -0.000000000000000000 ) ) ;
#32085=SURFACE_STYLE_FILL_AREA ( #20653 ) ;
#32131=CARTESIAN_POINT ( 'NONE',  ( 3.000000000000000000, -1.467624384280027172, 2.542000000000001592 ) ) ;
#32156=CIRCLE ( 'NONE', #14792, 2.541999999999999815 ) ;
#32202=ORIENTED_EDGE ( 'NONE', *, *, #17646, .F. ) ;
#32211=CIRCLE ( 'NONE', #20235, 2.541999999999999815 ) ;
#32215=ADVANCED_FACE ( 'NONE', ( #25483 ), #5799, .F. ) ;
#32232=EDGE_CURVE ( 'NONE', #36602, #29314, #8785, .T. ) ;
#32251=CIRCLE ( 'NONE', #12500, 3.000000000000001332 ) ;
#32252=EDGE_CURVE ( 'NONE', #17975, #25264, #11036, .T. ) ;
#32283=CARTESIAN_POINT ( 'NONE',  ( 3.000000000000000000, -1.467624384280027172, 2.542000000000001592 ) ) ;
#32288=CARTESIAN_POINT ( 'NONE',  ( 6.249999999999998224, 0.000000000000000000, 0.000000000000000000 ) ) ;
#32338=ADVANCED_FACE ( 'NONE', ( #6709 ), #26407, .T. ) ;
#32407=FILL_AREA_STYLE ('',( #29407 ) ) ;
#32438=DIRECTION ( 'NONE',  ( 0.000000000000000000, 0.000000000000000000, 1.000000000000000000 ) ) ;
#32448=ORIENTED_EDGE ( 'NONE', *, *, #14901, .F. ) ;
#32507=CARTESIAN_POINT ( 'NONE',  ( 35.99999999999999289, 0.000000000000000000, 0.000000000000000000 ) ) ;
#32579=ORIENTED_EDGE ( 'NONE', *, *, #16133, .T. ) ;
#32583=SURFACE_STYLE_FILL_AREA ( #32407 ) ;
#32589=ORIENTED_EDGE ( 'NONE', *, *, #25638, .F. ) ;
#32714=CARTESIAN_POINT ( 'NONE',  ( 6.000000000000000000, 0.000000000000000000, 0.000000000000000000 ) ) ;
#32717=EDGE_CURVE ( 'NONE', #31926, #19348, #20709, .T. ) ;
#32750=CLOSED_SHELL ( 'NONE', ( #31016, #5762, #22049, #27000, #20895, #32338, #22819, #31612, #21081, #29204, #11563, #187, #9885, #11460, #13218, #10162, #13832, #10254, #11546, #26463, #11023, #3370, #201, #32215, #20119, #18352, #26261 ) ) ;
#32923=ORIENTED_EDGE ( 'NONE', *, *, #9990, .F. ) ;
#32983=EDGE_CURVE ( 'NONE', #34152, #1959, #24930, .T. ) ;
#33234=ORIENTED_EDGE ( 'NONE', *, *, #9478, .F. ) ;
#33278=VECTOR ( 'NONE', #4065, 1000.000000000000000 ) ;
#33305=EDGE_CURVE ( 'NONE', #36242, #29705, #30959, .T. ) ;
#33318=ORIENTED_EDGE ( 'NONE', *, *, #2648, .T. ) ;
#33346=VECTOR ( 'NONE', #14484, 1000.000000000000000 ) ;
#33390=CARTESIAN_POINT ( 'NONE',  ( 3.000000000000000000, -1.467624384280027172, 2.542000000000001592 ) ) ;
#33396=CARTESIAN_POINT ( 'NONE',  ( 0.3000000000000016542, 0.000000000000000000, 0.000000000000000000 ) ) ;
#33488=ORIENTED_EDGE ( 'NONE', *, *, #25374, .F. ) ;
#33538=EDGE_CURVE ( 'NONE', #8984, #30547, #23266, .T. ) ;
#33551=CARTESIAN_POINT ( 'NONE',  ( 35.44550000000001688, 0.000000000000000000, 0.000000000000000000 ) ) ;
#33616=FACE_OUTER_BOUND ( 'NONE', #36285, .T. ) ;
#33652=ORIENTED_EDGE ( 'NONE', *, *, #36651, .T. ) ;
#33728=EDGE_CURVE ( 'NONE', #30219, #23050, #26819, .T. ) ;
#33729=EDGE_CURVE ( 'NONE', #29705, #25264, #32156, .T. ) ;
#33929=ORIENTED_EDGE ( 'NONE', *, *, #404, .T. ) ;
#33946=( NAMED_UNIT ( * ) PLANE_ANGLE_UNIT ( ) SI_UNIT ( $, .RADIAN. ) );
#33960=CARTESIAN_POINT ( 'NONE',  ( 3.000000000000000000, 4.131365146527188963E-15, 2.541999999999999371 ) ) ;
#33982=CIRCLE ( 'NONE', #14211, 2.445500000000000007 ) ;
#34090=VERTEX_POINT ( 'NONE', #4409 ) ;
#34104=DIRECTION ( 'NONE',  ( 0.000000000000000000, 0.000000000000000000, 1.000000000000000000 ) ) ;
#34112=EDGE_CURVE ( 'NONE', #5803, #1959, #10043, .T. ) ;
#34138=CARTESIAN_POINT ( 'NONE',  ( 3.000000000000000000, 2.935248768560057453, -3.903127820947815962E-15 ) ) ;
#34152=VERTEX_POINT ( 'NONE', #15666 ) ;
#34235=DIRECTION ( 'NONE',  ( -1.000000000000000000, -0.000000000000000000, -0.000000000000000000 ) ) ;
#34293=DIRECTION ( 'NONE',  ( 0.000000000000000000, 1.000000000000000000, -1.625241993126352989E-15 ) ) ;
#34494=ORIENTED_EDGE ( 'NONE', *, *, #17942, .F. ) ;
#34653=ORIENTED_EDGE ( 'NONE', *, *, #25374, .T. ) ;
#34777=ORIENTED_EDGE ( 'NONE', *, *, #33729, .F. ) ;
#34840=EDGE_CURVE ( 'NONE', #7880, #3751, #34893, .T. ) ;
#34893=LINE ( 'NONE', #20273, #5569 ) ;
#34965=LINE ( 'NONE', #32131, #18430 ) ;
#34988=EDGE_CURVE ( 'NONE', #25264, #26476, #16360, .T. ) ;
#35002=CARTESIAN_POINT ( 'NONE',  ( 3.000000000000000000, 0.000000000000000000, 0.000000000000000000 ) ) ;
#35050=VERTEX_POINT ( 'NONE', #36187 ) ;
#35074=DIRECTION ( 'NONE',  ( 0.000000000000000000, -1.000000000000000000, 1.034244904716769672E-15 ) ) ;
#35153=DIRECTION ( 'NONE',  ( 0.000000000000000000, 0.000000000000000000, -1.000000000000000000 ) ) ;
#35157=VECTOR ( 'NONE', #3034, 1000.000000000000000 ) ;
#35199=ORIENTED_EDGE ( 'NONE', *, *, #7731, .T. ) ;
#35249=SURFACE_SIDE_STYLE ('',( #32583 ) ) ;
#35313=CARTESIAN_POINT ( 'NONE',  ( 3.000000000000000000, 2.935248768560057453, -3.903127820947815962E-15 ) ) ;
#35366=CIRCLE ( 'NONE', #30549, 3.000000000000000888 ) ;
#35687=EDGE_LOOP ( 'NONE', ( #30262, #31805, #31978, #24919 ) ) ;
#35739=ORIENTED_EDGE ( 'NONE', *, *, #28504, .F. ) ;
#35798=MECHANICAL_DESIGN_GEOMETRIC_PRESENTATION_REPRESENTATION('',(#30992),#30898);
#35869=ORIENTED_EDGE ( 'NONE', *, *, #9478, .T. ) ;
#36016=CARTESIAN_POINT ( 'NONE',  ( 3.000000000000000000, 0.000000000000000000, 0.000000000000000000 ) ) ;
#36039=DIRECTION ( 'NONE',  ( 0.000000000000000000, 0.000000000000000000, 1.000000000000000000 ) ) ;
#36066=ORIENTED_EDGE ( 'NONE', *, *, #33728, .F. ) ;
#36070=ORIENTED_EDGE ( 'NONE', *, *, #32983, .F. ) ;
#36150=LINE ( 'NONE', #36346, #22121 ) ;
#36182=DIRECTION ( 'NONE',  ( -1.000000000000000000, -0.000000000000000000, -0.000000000000000000 ) ) ;
#36185=ORIENTED_EDGE ( 'NONE', *, *, #16870, .F. ) ;
#36187=CARTESIAN_POINT ( 'NONE',  ( 3.000000000000000000, 1.467624384280024730, -2.542000000000001592 ) ) ;
#36196=DIRECTION ( 'NONE',  ( -0.000000000000000000, 0.8660254037844391517, 0.4999999999999990563 ) ) ;
#36209=VECTOR ( 'NONE', #14064, 1000.000000000000000 ) ;
#36242=VERTEX_POINT ( 'NONE', #10147 ) ;
#36269=CIRCLE ( 'NONE', #13496, 2.541999999999999815 ) ;
#36285=EDGE_LOOP ( 'NONE', ( #4516, #36066, #12139, #12858, #33929 ) ) ;
#36346=CARTESIAN_POINT ( 'NONE',  ( 3.000000000000000000, 1.467624384280024730, -2.542000000000001592 ) ) ;
#36396=DIRECTION ( 'NONE',  ( 1.000000000000000000, 0.000000000000000000, 0.000000000000000000 ) ) ;
#36462=AXIS2_PLACEMENT_3D ( 'NONE', #5593, #17409, #12111 ) ;
#36465=EDGE_CURVE ( 'NONE', #31031, #16370, #36906, .T. ) ;
#36520=EDGE_LOOP ( 'NONE', ( #1487, #12157, #34777 ) ) ;
#36544=DIRECTION ( 'NONE',  ( 0.000000000000000000, 0.000000000000000000, -1.000000000000000000 ) ) ;
#36563=CARTESIAN_POINT ( 'NONE',  ( 5.999999999999999112, 3.980102097228899218E-16, 3.250000000000001332 ) ) ;
#36602=VERTEX_POINT ( 'NONE', #22618 ) ;
#36651=EDGE_CURVE ( 'NONE', #35050, #12167, #31056, .T. ) ;
#36678=DIRECTION ( 'NONE',  ( -1.000000000000000000, -0.000000000000000000, -0.000000000000000000 ) ) ;
#36707=DIRECTION ( 'NONE',  ( 1.000000000000000000, 0.000000000000000000, 0.000000000000000000 ) ) ;
#36751=CARTESIAN_POINT ( 'NONE',  ( 3.000000000000000000, 1.467624384280029615, 2.541999999999997151 ) ) ;
#36783=VERTEX_POINT ( 'NONE', #4249 ) ;
#36806=CARTESIAN_POINT ( 'NONE',  ( 3.000000000000000000, -2.935248768560059229, 3.469446951953614189E-15 ) ) ;
#36834=AXIS2_PLACEMENT_3D ( 'NONE', #7853, #36707, #36544 ) ;
#36906=CIRCLE ( 'NONE', #4586, 5.000000000000000000 ) ;
#36947=CARTESIAN_POINT ( 'NONE',  ( 0.3000000000000016542, 0.000000000000000000, 4.700000000000000178 ) ) ;
#37010=PRODUCT ( 'socket head cap screw_iso_ISO 4762 M6 x 30 - 30N', 'socket head cap screw_iso_ISO 4762 M6 x 30 - 30N', '', ( #3516 ) ) ;
#37012=AXIS2_PLACEMENT_3D ( 'NONE', #28534, #16918, #2662 ) ;
#37073=ORIENTED_EDGE ( 'NONE', *, *, #32717, .F. ) ;
ENDSEC;
END-ISO-10303-21;
